ISO-10303-21;
HEADER;
/* Generated by software containing ST-Developer
 * from STEP Tools, Inc. (www.steptools.com) 
 */

FILE_DESCRIPTION(
/* description */ ('Turntable on roller ring'),
/* implementation_level */ '2;1');

FILE_NAME(
/* name */ 'M5x14 Cap Screw.step',
/* time_stamp */ '2026-10-28T03:23:59-07:00',
/* author */ (''),
/* organization */ (''),
/* preprocessor_version */ 'ST-DEVELOPER v20.2',
/* originating_system */ 'Autodesk Translation Framework v15.17.0.0',
/* authorisation */ '');

FILE_SCHEMA (('AUTOMOTIVE_DESIGN { 1 0 10303 214 3 1 1 }'));
ENDSEC;

DATA;
#10=MECHANICAL_DESIGN_GEOMETRIC_PRESENTATION_REPRESENTATION('',(#662),#16281);
#489=CONICAL_SURFACE('',#9853,0.4,0.785398163397448);
#490=CONICAL_SURFACE('',#9857,0.41,0.785398163397448);
#491=CONICAL_SURFACE('',#9861,0.26,0.463647609000806);
#501=ORIENTED_CLOSED_SHELL('',*,#8405,.F.);
#505=BREP_WITH_VOIDS('Body1',#8406,(#501));
#543=SHAPE_REPRESENTATION_RELATIONSHIP('SRR','None',#16563,#598);
#598=ADVANCED_BREP_SHAPE_REPRESENTATION('',(#505),#16257);
#662=STYLED_ITEM('',(#16939),#505);
#955=FACE_BOUND('',#2341,.T.);
#1187=PLANE('',#9841);
#1188=PLANE('',#9842);
#1189=PLANE('',#9843);
#1190=PLANE('',#9844);
#1191=PLANE('',#9845);
#1192=PLANE('',#9846);
#1193=PLANE('',#9847);
#1194=PLANE('',#9848);
#1195=PLANE('',#9849);
#1196=PLANE('',#9851);
#1197=PLANE('',#9859);
#1624=FACE_OUTER_BOUND('',#2327,.T.);
#1625=FACE_OUTER_BOUND('',#2328,.T.);
#1626=FACE_OUTER_BOUND('',#2329,.T.);
#1627=FACE_OUTER_BOUND('',#2330,.T.);
#1628=FACE_OUTER_BOUND('',#2331,.T.);
#1629=FACE_OUTER_BOUND('',#2332,.T.);
#1630=FACE_OUTER_BOUND('',#2333,.T.);
#1631=FACE_OUTER_BOUND('',#2334,.T.);
#1632=FACE_OUTER_BOUND('',#2335,.T.);
#1633=FACE_OUTER_BOUND('',#2336,.T.);
#1634=FACE_OUTER_BOUND('',#2337,.T.);
#1635=FACE_OUTER_BOUND('',#2338,.T.);
#1636=FACE_OUTER_BOUND('',#2339,.T.);
#1637=FACE_OUTER_BOUND('',#2340,.T.);
#1638=FACE_OUTER_BOUND('',#2342,.T.);
#1639=FACE_OUTER_BOUND('',#2343,.T.);
#2327=EDGE_LOOP('',(#7193,#7194,#7195,#7196));
#2328=EDGE_LOOP('',(#7197,#7198,#7199,#7200));
#2329=EDGE_LOOP('',(#7201,#7202,#7203,#7204));
#2330=EDGE_LOOP('',(#7205,#7206,#7207,#7208));
#2331=EDGE_LOOP('',(#7209,#7210,#7211,#7212));
#2332=EDGE_LOOP('',(#7213,#7214,#7215,#7216));
#2333=EDGE_LOOP('',(#7217,#7218,#7219,#7220,#7221,#7222));
#2334=EDGE_LOOP('',(#7223,#7224,#7225,#7226,#7227,#7228));
#2335=EDGE_LOOP('',(#7229));
#2336=EDGE_LOOP('',(#7230));
#2337=EDGE_LOOP('',(#7231,#7232,#7233,#7234));
#2338=EDGE_LOOP('',(#7235,#7236,#7237,#7238));
#2339=EDGE_LOOP('',(#7239,#7240,#7241,#7242));
#2340=EDGE_LOOP('',(#7243));
#2341=EDGE_LOOP('',(#7244));
#2342=EDGE_LOOP('',(#7245,#7246,#7247,#7248));
#2343=EDGE_LOOP('',(#7249,#7250,#7251,#7252));
#2890=LINE('',#15180,#3373);
#2891=LINE('',#15182,#3374);
#2892=LINE('',#15184,#3375);
#2893=LINE('',#15185,#3376);
#2894=LINE('',#15188,#3377);
#2895=LINE('',#15190,#3378);
#2896=LINE('',#15191,#3379);
#2897=LINE('',#15194,#3380);
#2898=LINE('',#15196,#3381);
#2899=LINE('',#15197,#3382);
#2900=LINE('',#15200,#3383);
#2901=LINE('',#15202,#3384);
#2902=LINE('',#15203,#3385);
#2903=LINE('',#15206,#3386);
#2904=LINE('',#15208,#3387);
#2905=LINE('',#15209,#3388);
#2906=LINE('',#15211,#3389);
#2907=LINE('',#15212,#3390);
#2908=LINE('',#15224,#3391);
#2909=LINE('',#15228,#3392);
#2910=LINE('',#15232,#3393);
#2911=LINE('',#15239,#3394);
#2912=LINE('',#15241,#3395);
#3373=VECTOR('',#12201,1.);
#3374=VECTOR('',#12202,1.);
#3375=VECTOR('',#12203,1.);
#3376=VECTOR('',#12204,1.);
#3377=VECTOR('',#12207,1.);
#3378=VECTOR('',#12208,1.);
#3379=VECTOR('',#12209,1.);
#3380=VECTOR('',#12212,1.);
#3381=VECTOR('',#12213,1.);
#3382=VECTOR('',#12214,1.);
#3383=VECTOR('',#12217,1.);
#3384=VECTOR('',#12218,1.);
#3385=VECTOR('',#12219,1.);
#3386=VECTOR('',#12222,1.);
#3387=VECTOR('',#12223,1.);
#3388=VECTOR('',#12224,1.);
#3389=VECTOR('',#12227,1.);
#3390=VECTOR('',#12228,1.);
#3391=VECTOR('',#12245,0.4);
#3392=VECTOR('',#12250,0.425);
#3393=VECTOR('',#12255,0.41);
#3394=VECTOR('',#12264,0.26);
#3395=VECTOR('',#12267,0.25);
#3815=CIRCLE('',#9850,0.24505);
#3816=CIRCLE('',#9852,0.375);
#3817=CIRCLE('',#9854,0.425);
#3818=CIRCLE('',#9856,0.425);
#3819=CIRCLE('',#9858,0.395);
#3820=CIRCLE('',#9860,0.27);
#3821=CIRCLE('',#9862,0.24505);
#4467=VERTEX_POINT('',#15178);
#4468=VERTEX_POINT('',#15179);
#4469=VERTEX_POINT('',#15181);
#4470=VERTEX_POINT('',#15183);
#4471=VERTEX_POINT('',#15187);
#4472=VERTEX_POINT('',#15189);
#4473=VERTEX_POINT('',#15193);
#4474=VERTEX_POINT('',#15195);
#4475=VERTEX_POINT('',#15199);
#4476=VERTEX_POINT('',#15201);
#4477=VERTEX_POINT('',#15205);
#4478=VERTEX_POINT('',#15207);
#4479=VERTEX_POINT('',#15216);
#4480=VERTEX_POINT('',#15219);
#4481=VERTEX_POINT('',#15222);
#4482=VERTEX_POINT('',#15226);
#4483=VERTEX_POINT('',#15230);
#4484=VERTEX_POINT('',#15234);
#4485=VERTEX_POINT('',#15237);
#5407=EDGE_CURVE('',#4467,#4468,#2890,.T.);
#5408=EDGE_CURVE('',#4468,#4469,#2891,.T.);
#5409=EDGE_CURVE('',#4469,#4470,#2892,.T.);
#5410=EDGE_CURVE('',#4467,#4470,#2893,.T.);
#5411=EDGE_CURVE('',#4468,#4471,#2894,.T.);
#5412=EDGE_CURVE('',#4471,#4472,#2895,.T.);
#5413=EDGE_CURVE('',#4472,#4469,#2896,.T.);
#5414=EDGE_CURVE('',#4471,#4473,#2897,.T.);
#5415=EDGE_CURVE('',#4473,#4474,#2898,.T.);
#5416=EDGE_CURVE('',#4474,#4472,#2899,.T.);
#5417=EDGE_CURVE('',#4473,#4475,#2900,.T.);
#5418=EDGE_CURVE('',#4475,#4476,#2901,.T.);
#5419=EDGE_CURVE('',#4476,#4474,#2902,.T.);
#5420=EDGE_CURVE('',#4475,#4477,#2903,.T.);
#5421=EDGE_CURVE('',#4477,#4478,#2904,.T.);
#5422=EDGE_CURVE('',#4478,#4476,#2905,.T.);
#5423=EDGE_CURVE('',#4477,#4467,#2906,.T.);
#5424=EDGE_CURVE('',#4470,#4478,#2907,.T.);
#5425=EDGE_CURVE('',#4479,#4479,#3815,.T.);
#5426=EDGE_CURVE('',#4480,#4480,#3816,.T.);
#5427=EDGE_CURVE('',#4481,#4481,#3817,.T.);
#5428=EDGE_CURVE('',#4481,#4480,#2908,.T.);
#5429=EDGE_CURVE('',#4482,#4482,#3818,.T.);
#5430=EDGE_CURVE('',#4482,#4481,#2909,.T.);
#5431=EDGE_CURVE('',#4483,#4483,#3819,.T.);
#5432=EDGE_CURVE('',#4483,#4482,#2910,.T.);
#5433=EDGE_CURVE('',#4484,#4484,#3820,.T.);
#5434=EDGE_CURVE('',#4485,#4485,#3821,.F.);
#5435=EDGE_CURVE('',#4485,#4484,#2911,.T.);
#5436=EDGE_CURVE('',#4479,#4485,#2912,.T.);
#7193=ORIENTED_EDGE('',*,*,#5407,.T.);
#7194=ORIENTED_EDGE('',*,*,#5408,.T.);
#7195=ORIENTED_EDGE('',*,*,#5409,.T.);
#7196=ORIENTED_EDGE('',*,*,#5410,.F.);
#7197=ORIENTED_EDGE('',*,*,#5411,.T.);
#7198=ORIENTED_EDGE('',*,*,#5412,.T.);
#7199=ORIENTED_EDGE('',*,*,#5413,.T.);
#7200=ORIENTED_EDGE('',*,*,#5408,.F.);
#7201=ORIENTED_EDGE('',*,*,#5414,.T.);
#7202=ORIENTED_EDGE('',*,*,#5415,.T.);
#7203=ORIENTED_EDGE('',*,*,#5416,.T.);
#7204=ORIENTED_EDGE('',*,*,#5412,.F.);
#7205=ORIENTED_EDGE('',*,*,#5417,.T.);
#7206=ORIENTED_EDGE('',*,*,#5418,.T.);
#7207=ORIENTED_EDGE('',*,*,#5419,.T.);
#7208=ORIENTED_EDGE('',*,*,#5415,.F.);
#7209=ORIENTED_EDGE('',*,*,#5420,.T.);
#7210=ORIENTED_EDGE('',*,*,#5421,.T.);
#7211=ORIENTED_EDGE('',*,*,#5422,.T.);
#7212=ORIENTED_EDGE('',*,*,#5418,.F.);
#7213=ORIENTED_EDGE('',*,*,#5423,.T.);
#7214=ORIENTED_EDGE('',*,*,#5410,.T.);
#7215=ORIENTED_EDGE('',*,*,#5424,.T.);
#7216=ORIENTED_EDGE('',*,*,#5421,.F.);
#7217=ORIENTED_EDGE('',*,*,#5423,.F.);
#7218=ORIENTED_EDGE('',*,*,#5420,.F.);
#7219=ORIENTED_EDGE('',*,*,#5417,.F.);
#7220=ORIENTED_EDGE('',*,*,#5414,.F.);
#7221=ORIENTED_EDGE('',*,*,#5411,.F.);
#7222=ORIENTED_EDGE('',*,*,#5407,.F.);
#7223=ORIENTED_EDGE('',*,*,#5424,.F.);
#7224=ORIENTED_EDGE('',*,*,#5409,.F.);
#7225=ORIENTED_EDGE('',*,*,#5413,.F.);
#7226=ORIENTED_EDGE('',*,*,#5416,.F.);
#7227=ORIENTED_EDGE('',*,*,#5419,.F.);
#7228=ORIENTED_EDGE('',*,*,#5422,.F.);
#7229=ORIENTED_EDGE('',*,*,#5425,.F.);
#7230=ORIENTED_EDGE('',*,*,#5426,.F.);
#7231=ORIENTED_EDGE('',*,*,#5427,.F.);
#7232=ORIENTED_EDGE('',*,*,#5428,.T.);
#7233=ORIENTED_EDGE('',*,*,#5426,.T.);
#7234=ORIENTED_EDGE('',*,*,#5428,.F.);
#7235=ORIENTED_EDGE('',*,*,#5429,.F.);
#7236=ORIENTED_EDGE('',*,*,#5430,.T.);
#7237=ORIENTED_EDGE('',*,*,#5427,.T.);
#7238=ORIENTED_EDGE('',*,*,#5430,.F.);
#7239=ORIENTED_EDGE('',*,*,#5431,.F.);
#7240=ORIENTED_EDGE('',*,*,#5432,.T.);
#7241=ORIENTED_EDGE('',*,*,#5429,.T.);
#7242=ORIENTED_EDGE('',*,*,#5432,.F.);
#7243=ORIENTED_EDGE('',*,*,#5431,.T.);
#7244=ORIENTED_EDGE('',*,*,#5433,.F.);
#7245=ORIENTED_EDGE('',*,*,#5434,.F.);
#7246=ORIENTED_EDGE('',*,*,#5435,.T.);
#7247=ORIENTED_EDGE('',*,*,#5433,.T.);
#7248=ORIENTED_EDGE('',*,*,#5435,.F.);
#7249=ORIENTED_EDGE('',*,*,#5425,.T.);
#7250=ORIENTED_EDGE('',*,*,#5436,.T.);
#7251=ORIENTED_EDGE('',*,*,#5434,.T.);
#7252=ORIENTED_EDGE('',*,*,#5436,.F.);
#7813=CYLINDRICAL_SURFACE('',#9855,0.425);
#7814=CYLINDRICAL_SURFACE('',#9863,0.24505);
#8227=ADVANCED_FACE('',(#1624),#1187,.F.);
#8228=ADVANCED_FACE('',(#1625),#1188,.F.);
#8229=ADVANCED_FACE('',(#1626),#1189,.F.);
#8230=ADVANCED_FACE('',(#1627),#1190,.F.);
#8231=ADVANCED_FACE('',(#1628),#1191,.F.);
#8232=ADVANCED_FACE('',(#1629),#1192,.F.);
#8233=ADVANCED_FACE('',(#1630),#1193,.F.);
#8234=ADVANCED_FACE('',(#1631),#1194,.F.);
#8235=ADVANCED_FACE('',(#1632),#1195,.F.);
#8236=ADVANCED_FACE('',(#1633),#1196,.T.);
#8237=ADVANCED_FACE('',(#1634),#489,.T.);
#8238=ADVANCED_FACE('',(#1635),#7813,.T.);
#8239=ADVANCED_FACE('',(#1636),#490,.T.);
#8240=ADVANCED_FACE('',(#1637,#955),#1197,.T.);
#8241=ADVANCED_FACE('',(#1638),#491,.T.);
#8242=ADVANCED_FACE('',(#1639),#7814,.T.);
#8405=CLOSED_SHELL('',(#8227,#8228,#8229,#8230,#8231,#8232,#8233,#8234));
#8406=CLOSED_SHELL('',(#8235,#8236,#8237,#8238,#8239,#8240,#8241,#8242));
#9840=AXIS2_PLACEMENT_3D('',#15176,#12197,#12198);
#9841=AXIS2_PLACEMENT_3D('',#15177,#12199,#12200);
#9842=AXIS2_PLACEMENT_3D('',#15186,#12205,#12206);
#9843=AXIS2_PLACEMENT_3D('',#15192,#12210,#12211);
#9844=AXIS2_PLACEMENT_3D('',#15198,#12215,#12216);
#9845=AXIS2_PLACEMENT_3D('',#15204,#12220,#12221);
#9846=AXIS2_PLACEMENT_3D('',#15210,#12225,#12226);
#9847=AXIS2_PLACEMENT_3D('',#15213,#12229,#12230);
#9848=AXIS2_PLACEMENT_3D('',#15214,#12231,#12232);
#9849=AXIS2_PLACEMENT_3D('',#15215,#12233,#12234);
#9850=AXIS2_PLACEMENT_3D('',#15217,#12235,#12236);
#9851=AXIS2_PLACEMENT_3D('',#15218,#12237,#12238);
#9852=AXIS2_PLACEMENT_3D('',#15220,#12239,#12240);
#9853=AXIS2_PLACEMENT_3D('',#15221,#12241,#12242);
#9854=AXIS2_PLACEMENT_3D('',#15223,#12243,#12244);
#9855=AXIS2_PLACEMENT_3D('',#15225,#12246,#12247);
#9856=AXIS2_PLACEMENT_3D('',#15227,#12248,#12249);
#9857=AXIS2_PLACEMENT_3D('',#15229,#12251,#12252);
#9858=AXIS2_PLACEMENT_3D('',#15231,#12253,#12254);
#9859=AXIS2_PLACEMENT_3D('',#15233,#12256,#12257);
#9860=AXIS2_PLACEMENT_3D('',#15235,#12258,#12259);
#9861=AXIS2_PLACEMENT_3D('',#15236,#12260,#12261);
#9862=AXIS2_PLACEMENT_3D('',#15238,#12262,#12263);
#9863=AXIS2_PLACEMENT_3D('',#15240,#12265,#12266);
#12197=DIRECTION('axis',(0.,0.,1.));
#12198=DIRECTION('refdir',(1.,0.,0.));
#12199=DIRECTION('center_axis',(0.866025403784439,0.,-0.5));
#12200=DIRECTION('ref_axis',(0.5,0.,0.866025403784439));
#12201=DIRECTION('',(-0.5,0.,-0.866025403784439));
#12202=DIRECTION('',(0.,-1.,0.));
#12203=DIRECTION('',(0.5,0.,0.866025403784439));
#12204=DIRECTION('',(0.,-1.,0.));
#12205=DIRECTION('center_axis',(1.20185167898973E-16,0.,-1.));
#12206=DIRECTION('ref_axis',(1.,0.,1.20185167898973E-16));
#12207=DIRECTION('',(-1.,0.,-1.20185167898973E-16));
#12208=DIRECTION('',(0.,-1.,0.));
#12209=DIRECTION('',(1.,0.,1.20185167898973E-16));
#12210=DIRECTION('center_axis',(-0.866025403784439,0.,-0.5));
#12211=DIRECTION('ref_axis',(0.5,0.,-0.866025403784439));
#12212=DIRECTION('',(-0.5,0.,0.866025403784439));
#12213=DIRECTION('',(0.,-1.,0.));
#12214=DIRECTION('',(0.5,0.,-0.866025403784439));
#12215=DIRECTION('center_axis',(-0.866025403784439,0.,0.5));
#12216=DIRECTION('ref_axis',(-0.5,0.,-0.866025403784439));
#12217=DIRECTION('',(0.5,0.,0.866025403784439));
#12218=DIRECTION('',(0.,-1.,0.));
#12219=DIRECTION('',(-0.5,0.,-0.866025403784439));
#12220=DIRECTION('center_axis',(-2.40370335797945E-16,0.,1.));
#12221=DIRECTION('ref_axis',(-1.,0.,-2.40370335797945E-16));
#12222=DIRECTION('',(1.,0.,2.40370335797945E-16));
#12223=DIRECTION('',(0.,-1.,0.));
#12224=DIRECTION('',(-1.,0.,-2.40370335797945E-16));
#12225=DIRECTION('center_axis',(0.866025403784439,0.,0.5));
#12226=DIRECTION('ref_axis',(-0.5,0.,0.866025403784439));
#12227=DIRECTION('',(0.5,0.,-0.866025403784439));
#12228=DIRECTION('',(-0.5,0.,0.866025403784439));
#12229=DIRECTION('center_axis',(0.,1.,0.));
#12230=DIRECTION('ref_axis',(1.,0.,0.));
#12231=DIRECTION('center_axis',(0.,-1.,0.));
#12232=DIRECTION('ref_axis',(0.,0.,-1.));
#12233=DIRECTION('center_axis',(0.,1.,0.));
#12234=DIRECTION('ref_axis',(1.,0.,0.));
#12235=DIRECTION('center_axis',(0.,1.,0.));
#12236=DIRECTION('ref_axis',(1.,0.,0.));
#12237=DIRECTION('center_axis',(0.,1.,0.));
#12238=DIRECTION('ref_axis',(0.,0.,1.));
#12239=DIRECTION('center_axis',(0.,-1.,0.));
#12240=DIRECTION('ref_axis',(1.,0.,0.));
#12241=DIRECTION('center_axis',(0.,-1.,0.));
#12242=DIRECTION('ref_axis',(1.,0.,0.));
#12243=DIRECTION('center_axis',(0.,-1.,0.));
#12244=DIRECTION('ref_axis',(1.,0.,0.));
#12245=DIRECTION('',(0.707106781186548,0.707106781186547,8.65956056235493E-17));
#12246=DIRECTION('center_axis',(0.,-1.,0.));
#12247=DIRECTION('ref_axis',(1.,0.,0.));
#12248=DIRECTION('center_axis',(0.,-1.,0.));
#12249=DIRECTION('ref_axis',(1.,0.,0.));
#12250=DIRECTION('',(0.,1.,0.));
#12251=DIRECTION('center_axis',(0.,1.,0.));
#12252=DIRECTION('ref_axis',(1.,0.,0.));
#12253=DIRECTION('center_axis',(0.,-1.,0.));
#12254=DIRECTION('ref_axis',(1.,0.,0.));
#12255=DIRECTION('',(-0.707106781186547,0.707106781186548,-8.65956056235493E-17));
#12256=DIRECTION('center_axis',(0.,-1.,0.));
#12257=DIRECTION('ref_axis',(0.,0.,-1.));
#12258=DIRECTION('center_axis',(0.,-1.,0.));
#12259=DIRECTION('ref_axis',(1.,0.,0.));
#12260=DIRECTION('center_axis',(0.,1.,0.));
#12261=DIRECTION('ref_axis',(1.,0.,0.));
#12262=DIRECTION('center_axis',(0.,1.,0.));
#12263=DIRECTION('ref_axis',(1.,0.,0.));
#12264=DIRECTION('',(-0.447213595499958,0.894427190999916,-5.47678698264203E-17));
#12265=DIRECTION('center_axis',(0.,-1.,0.));
#12266=DIRECTION('ref_axis',(1.,0.,0.));
#12267=DIRECTION('',(0.,1.,0.));
#15176=CARTESIAN_POINT('',(0.,0.,0.));
#15177=CARTESIAN_POINT('Origin',(0.115470053837925,-0.5,-0.2));
#15178=CARTESIAN_POINT('',(0.23094010767585,-0.5,0.));
#15179=CARTESIAN_POINT('',(0.115470053837925,-0.5,-0.2));
#15180=CARTESIAN_POINT('',(0.23094010767585,-0.5,0.));
#15181=CARTESIAN_POINT('',(0.115470053837925,-0.8,-0.2));
#15182=CARTESIAN_POINT('',(0.115470053837925,-0.5,-0.2));
#15183=CARTESIAN_POINT('',(0.23094010767585,-0.8,0.));
#15184=CARTESIAN_POINT('',(0.23094010767585,-0.8,0.));
#15185=CARTESIAN_POINT('',(0.23094010767585,-0.5,0.));
#15186=CARTESIAN_POINT('Origin',(-0.115470053837925,-0.5,-0.2));
#15187=CARTESIAN_POINT('',(-0.115470053837925,-0.5,-0.2));
#15188=CARTESIAN_POINT('',(0.115470053837925,-0.5,-0.2));
#15189=CARTESIAN_POINT('',(-0.115470053837925,-0.8,-0.2));
#15190=CARTESIAN_POINT('',(-0.115470053837925,-0.5,-0.2));
#15191=CARTESIAN_POINT('',(0.115470053837925,-0.8,-0.2));
#15192=CARTESIAN_POINT('Origin',(-0.23094010767585,-0.5,-2.77555756156289E-17));
#15193=CARTESIAN_POINT('',(-0.23094010767585,-0.5,-2.82820063659975E-17));
#15194=CARTESIAN_POINT('',(-0.115470053837925,-0.5,-0.2));
#15195=CARTESIAN_POINT('',(-0.23094010767585,-0.8,-2.77555756156289E-17));
#15196=CARTESIAN_POINT('',(-0.23094010767585,-0.5,-2.82820063659975E-17));
#15197=CARTESIAN_POINT('',(-0.115470053837925,-0.8,-0.2));
#15198=CARTESIAN_POINT('Origin',(-0.115470053837925,-0.5,0.2));
#15199=CARTESIAN_POINT('',(-0.115470053837925,-0.5,0.2));
#15200=CARTESIAN_POINT('',(-0.23094010767585,-0.5,-2.82820063659975E-17));
#15201=CARTESIAN_POINT('',(-0.115470053837925,-0.8,0.2));
#15202=CARTESIAN_POINT('',(-0.115470053837925,-0.5,0.2));
#15203=CARTESIAN_POINT('',(-0.23094010767585,-0.8,-2.82820063659975E-17));
#15204=CARTESIAN_POINT('Origin',(0.115470053837925,-0.5,0.2));
#15205=CARTESIAN_POINT('',(0.115470053837925,-0.5,0.2));
#15206=CARTESIAN_POINT('',(-0.115470053837925,-0.5,0.2));
#15207=CARTESIAN_POINT('',(0.115470053837925,-0.8,0.2));
#15208=CARTESIAN_POINT('',(0.115470053837925,-0.5,0.2));
#15209=CARTESIAN_POINT('',(-0.115470053837925,-0.8,0.2));
#15210=CARTESIAN_POINT('Origin',(0.23094010767585,-0.5,0.));
#15211=CARTESIAN_POINT('',(0.115470053837925,-0.5,0.2));
#15212=CARTESIAN_POINT('',(0.115470053837925,-0.8,0.2));
#15213=CARTESIAN_POINT('Origin',(0.,-0.5,0.));
#15214=CARTESIAN_POINT('Origin',(0.,-0.8,0.));
#15215=CARTESIAN_POINT('Origin',(0.,-1.4,0.));
#15216=CARTESIAN_POINT('',(-0.24505,-1.4,3.00099698131059E-17));
#15217=CARTESIAN_POINT('Origin',(0.,-1.4,0.));
#15218=CARTESIAN_POINT('Origin',(0.375,0.5,0.));
#15219=CARTESIAN_POINT('',(-0.375,0.5,-4.59242549680257E-17));
#15220=CARTESIAN_POINT('Origin',(0.,0.5,0.));
#15221=CARTESIAN_POINT('Origin',(0.,0.475,0.));
#15222=CARTESIAN_POINT('',(-0.425,0.45,-5.20474889637625E-17));
#15223=CARTESIAN_POINT('Origin',(0.,0.45,0.));
#15224=CARTESIAN_POINT('',(-0.4,0.475,-4.89858719658941E-17));
#15225=CARTESIAN_POINT('Origin',(0.,0.24,0.));
#15226=CARTESIAN_POINT('',(-0.425,0.0299999999999998,-5.20474889637625E-17));
#15227=CARTESIAN_POINT('Origin',(0.,0.0299999999999998,0.));
#15228=CARTESIAN_POINT('',(-0.425,0.24,-5.20474889637625E-17));
#15229=CARTESIAN_POINT('Origin',(0.,0.0150000000000001,0.));
#15230=CARTESIAN_POINT('',(-0.395,4.85722573273506E-17,-4.83735485663204E-17));
#15231=CARTESIAN_POINT('Origin',(0.,0.,0.));
#15232=CARTESIAN_POINT('',(-0.41,0.0150000000000001,-5.02105187650415E-17));
#15233=CARTESIAN_POINT('Origin',(0.27,0.,0.));
#15234=CARTESIAN_POINT('',(-0.27,0.,-3.30654635769785E-17));
#15235=CARTESIAN_POINT('Origin',(0.,0.,0.));
#15236=CARTESIAN_POINT('Origin',(0.,-0.02,0.));
#15237=CARTESIAN_POINT('',(-0.24505,-0.0498999999999999,3.00099698131059E-17));
#15238=CARTESIAN_POINT('Origin',(0.,-0.0498999999999999,0.));
#15239=CARTESIAN_POINT('',(-0.26,-0.02,-3.18408167778312E-17));
#15240=CARTESIAN_POINT('Origin',(0.,-0.995,0.));
#15241=CARTESIAN_POINT('',(-0.24505,-0.995,-3.00099698131059E-17));
#16188=UNCERTAINTY_MEASURE_WITH_UNIT(LENGTH_MEASURE(0.001),#16282,
'DISTANCE_ACCURACY_VALUE',
'Maximum model space distance between geometric entities at asserted c
onnectivities');
#16212=UNCERTAINTY_MEASURE_WITH_UNIT(LENGTH_MEASURE(0.001),#16282,
'DISTANCE_ACCURACY_VALUE',
'Maximum model space distance between geometric entities at asserted c
onnectivities');
#16257=(
GEOMETRIC_REPRESENTATION_CONTEXT(3)
GLOBAL_UNCERTAINTY_ASSIGNED_CONTEXT((#16188))
GLOBAL_UNIT_ASSIGNED_CONTEXT((#16282,#16284,#16285))
REPRESENTATION_CONTEXT('','3D')
);
#16281=(
GEOMETRIC_REPRESENTATION_CONTEXT(3)
GLOBAL_UNCERTAINTY_ASSIGNED_CONTEXT((#16212))
GLOBAL_UNIT_ASSIGNED_CONTEXT((#16282,#16284,#16285))
REPRESENTATION_CONTEXT('','3D')
);
#16282=(
LENGTH_UNIT()
NAMED_UNIT(*)
SI_UNIT(.CENTI.,.METRE.)
);
#16284=(
NAMED_UNIT(*)
PLANE_ANGLE_UNIT()
SI_UNIT($,.RADIAN.)
);
#16285=(
NAMED_UNIT(*)
SI_UNIT($,.STERADIAN.)
SOLID_ANGLE_UNIT()
);
#16330=SHAPE_DEFINITION_REPRESENTATION(#16424,#16563);
#16424=PRODUCT_DEFINITION_SHAPE('',$,#16632);
#16563=SHAPE_REPRESENTATION('',(#9840),#16257);
#16587=PRODUCT_DEFINITION_CONTEXT('part definition',#16793,'design');
#16632=PRODUCT_DEFINITION('M5x14 Cap Screw','M5x14 Cap Screw',#16700,#16587);
#16700=PRODUCT_DEFINITION_FORMATION('',$,#16839);
#16793=APPLICATION_CONTEXT(
'Core Data for Automotive Mechanical Design Process');
#16794=PRODUCT_CONTEXT('part definition',#16793,'mechanical');
#16839=PRODUCT('M5x14 Cap Screw','M5x14 Cap Screw','M5x14 Cap Screw',(#16794));
#16933=COLOUR_RGB('Black',0.12,0.14,0.17);
#16934=FILL_AREA_STYLE_COLOUR('',#16933);
#16935=FILL_AREA_STYLE('',(#16934));
#16936=SURFACE_STYLE_FILL_AREA(#16935);
#16937=SURFACE_SIDE_STYLE('',(#16936));
#16938=SURFACE_STYLE_USAGE(.BOTH.,#16937);
#16939=PRESENTATION_STYLE_ASSIGNMENT((#16938));
ENDSEC;
END-ISO-10303-21;
